ISO-10303-21;
HEADER;
/* Generated by software containing ST-Developer
 * from STEP Tools, Inc. (www.steptools.com) 
 */

FILE_DESCRIPTION(
/* description */ ('Crank-driven oscillating fan base (mechanism only)'),

/* implementation_level */ '2;1');

FILE_NAME(
/* name */ 'M4x4 collar screw.step',
/* time_stamp */ '2026-10-28T03:25:00-07:00',
/* author */ (''),
/* organization */ (''),
/* preprocessor_version */ 'ST-DEVELOPER v20.2',
/* originating_system */ 'Autodesk Translation Framework v15.17.0.0',
/* authorisation */ '');

FILE_SCHEMA (('AUTOMOTIVE_DESIGN { 1 0 10303 214 3 1 1 }'));
ENDSEC;

DATA;
#10=MECHANICAL_DESIGN_GEOMETRIC_PRESENTATION_REPRESENTATION('',(#479),#11916);
#302=CONICAL_SURFACE('',#7261,0.185,0.785398163397449);
#391=SHAPE_REPRESENTATION_RELATIONSHIP('SRR','None',#12118,#431);
#431=ADVANCED_BREP_SHAPE_REPRESENTATION('',(#526),#11909);
#479=STYLED_ITEM('',(#12382),#526);
#526=MANIFOLD_SOLID_BREP('Body1',#6110);
#681=FACE_BOUND('',#1736,.T.);
#847=PLANE('',#7250);
#848=PLANE('',#7252);
#849=PLANE('',#7253);
#850=PLANE('',#7254);
#851=PLANE('',#7255);
#852=PLANE('',#7256);
#853=PLANE('',#7257);
#854=PLANE('',#7258);
#855=PLANE('',#7259);
#1201=FACE_OUTER_BOUND('',#1727,.T.);
#1202=FACE_OUTER_BOUND('',#1728,.T.);
#1203=FACE_OUTER_BOUND('',#1729,.T.);
#1204=FACE_OUTER_BOUND('',#1730,.T.);
#1205=FACE_OUTER_BOUND('',#1731,.T.);
#1206=FACE_OUTER_BOUND('',#1732,.T.);
#1207=FACE_OUTER_BOUND('',#1733,.T.);
#1208=FACE_OUTER_BOUND('',#1734,.T.);
#1209=FACE_OUTER_BOUND('',#1735,.T.);
#1210=FACE_OUTER_BOUND('',#1737,.T.);
#1211=FACE_OUTER_BOUND('',#1738,.T.);
#1727=EDGE_LOOP('',(#5316));
#1728=EDGE_LOOP('',(#5317,#5318,#5319,#5320));
#1729=EDGE_LOOP('',(#5321,#5322,#5323,#5324));
#1730=EDGE_LOOP('',(#5325,#5326,#5327,#5328));
#1731=EDGE_LOOP('',(#5329,#5330,#5331,#5332));
#1732=EDGE_LOOP('',(#5333,#5334,#5335,#5336));
#1733=EDGE_LOOP('',(#5337,#5338,#5339,#5340));
#1734=EDGE_LOOP('',(#5341,#5342,#5343,#5344,#5345,#5346));
#1735=EDGE_LOOP('',(#5347));
#1736=EDGE_LOOP('',(#5348,#5349,#5350,#5351,#5352,#5353));
#1737=EDGE_LOOP('',(#5354,#5355,#5356,#5357));
#1738=EDGE_LOOP('',(#5358,#5359,#5360,#5361));
#2050=LINE('',#11513,#2383);
#2051=LINE('',#11515,#2384);
#2052=LINE('',#11517,#2385);
#2053=LINE('',#11518,#2386);
#2054=LINE('',#11521,#2387);
#2055=LINE('',#11523,#2388);
#2056=LINE('',#11524,#2389);
#2057=LINE('',#11527,#2390);
#2058=LINE('',#11529,#2391);
#2059=LINE('',#11530,#2392);
#2060=LINE('',#11533,#2393);
#2061=LINE('',#11535,#2394);
#2062=LINE('',#11536,#2395);
#2063=LINE('',#11539,#2396);
#2064=LINE('',#11541,#2397);
#2065=LINE('',#11542,#2398);
#2066=LINE('',#11544,#2399);
#2067=LINE('',#11545,#2400);
#2068=LINE('',#11553,#2401);
#2069=LINE('',#11555,#2402);
#2383=VECTOR('',#9051,1.);
#2384=VECTOR('',#9052,1.);
#2385=VECTOR('',#9053,1.);
#2386=VECTOR('',#9054,1.);
#2387=VECTOR('',#9057,1.);
#2388=VECTOR('',#9058,1.);
#2389=VECTOR('',#9059,1.);
#2390=VECTOR('',#9062,1.);
#2391=VECTOR('',#9063,1.);
#2392=VECTOR('',#9064,1.);
#2393=VECTOR('',#9067,1.);
#2394=VECTOR('',#9068,1.);
#2395=VECTOR('',#9069,1.);
#2396=VECTOR('',#9072,1.);
#2397=VECTOR('',#9073,1.);
#2398=VECTOR('',#9074,1.);
#2399=VECTOR('',#9077,1.);
#2400=VECTOR('',#9078,1.);
#2401=VECTOR('',#9089,0.185);
#2402=VECTOR('',#9092,0.2);
#2795=CIRCLE('',#7251,0.1954);
#2796=CIRCLE('',#7260,0.17);
#2797=CIRCLE('',#7262,0.1954);
#3255=VERTEX_POINT('',#11508);
#3256=VERTEX_POINT('',#11511);
#3257=VERTEX_POINT('',#11512);
#3258=VERTEX_POINT('',#11514);
#3259=VERTEX_POINT('',#11516);
#3260=VERTEX_POINT('',#11520);
#3261=VERTEX_POINT('',#11522);
#3262=VERTEX_POINT('',#11526);
#3263=VERTEX_POINT('',#11528);
#3264=VERTEX_POINT('',#11532);
#3265=VERTEX_POINT('',#11534);
#3266=VERTEX_POINT('',#11538);
#3267=VERTEX_POINT('',#11540);
#3268=VERTEX_POINT('',#11548);
#3269=VERTEX_POINT('',#11551);
#3953=EDGE_CURVE('',#3255,#3255,#2795,.T.);
#3954=EDGE_CURVE('',#3256,#3257,#2050,.T.);
#3955=EDGE_CURVE('',#3256,#3258,#2051,.T.);
#3956=EDGE_CURVE('',#3258,#3259,#2052,.T.);
#3957=EDGE_CURVE('',#3257,#3259,#2053,.T.);
#3958=EDGE_CURVE('',#3260,#3256,#2054,.T.);
#3959=EDGE_CURVE('',#3260,#3261,#2055,.T.);
#3960=EDGE_CURVE('',#3261,#3258,#2056,.T.);
#3961=EDGE_CURVE('',#3262,#3260,#2057,.T.);
#3962=EDGE_CURVE('',#3262,#3263,#2058,.T.);
#3963=EDGE_CURVE('',#3263,#3261,#2059,.T.);
#3964=EDGE_CURVE('',#3264,#3262,#2060,.T.);
#3965=EDGE_CURVE('',#3264,#3265,#2061,.T.);
#3966=EDGE_CURVE('',#3265,#3263,#2062,.T.);
#3967=EDGE_CURVE('',#3266,#3264,#2063,.T.);
#3968=EDGE_CURVE('',#3266,#3267,#2064,.T.);
#3969=EDGE_CURVE('',#3267,#3265,#2065,.T.);
#3970=EDGE_CURVE('',#3257,#3266,#2066,.T.);
#3971=EDGE_CURVE('',#3259,#3267,#2067,.T.);
#3972=EDGE_CURVE('',#3268,#3268,#2796,.T.);
#3973=EDGE_CURVE('',#3269,#3269,#2797,.T.);
#3974=EDGE_CURVE('',#3269,#3268,#2068,.T.);
#3975=EDGE_CURVE('',#3255,#3269,#2069,.T.);
#5316=ORIENTED_EDGE('',*,*,#3953,.F.);
#5317=ORIENTED_EDGE('',*,*,#3954,.F.);
#5318=ORIENTED_EDGE('',*,*,#3955,.T.);
#5319=ORIENTED_EDGE('',*,*,#3956,.T.);
#5320=ORIENTED_EDGE('',*,*,#3957,.F.);
#5321=ORIENTED_EDGE('',*,*,#3958,.F.);
#5322=ORIENTED_EDGE('',*,*,#3959,.T.);
#5323=ORIENTED_EDGE('',*,*,#3960,.T.);
#5324=ORIENTED_EDGE('',*,*,#3955,.F.);
#5325=ORIENTED_EDGE('',*,*,#3961,.F.);
#5326=ORIENTED_EDGE('',*,*,#3962,.T.);
#5327=ORIENTED_EDGE('',*,*,#3963,.T.);
#5328=ORIENTED_EDGE('',*,*,#3959,.F.);
#5329=ORIENTED_EDGE('',*,*,#3964,.F.);
#5330=ORIENTED_EDGE('',*,*,#3965,.T.);
#5331=ORIENTED_EDGE('',*,*,#3966,.T.);
#5332=ORIENTED_EDGE('',*,*,#3962,.F.);
#5333=ORIENTED_EDGE('',*,*,#3967,.F.);
#5334=ORIENTED_EDGE('',*,*,#3968,.T.);
#5335=ORIENTED_EDGE('',*,*,#3969,.T.);
#5336=ORIENTED_EDGE('',*,*,#3965,.F.);
#5337=ORIENTED_EDGE('',*,*,#3970,.F.);
#5338=ORIENTED_EDGE('',*,*,#3957,.T.);
#5339=ORIENTED_EDGE('',*,*,#3971,.T.);
#5340=ORIENTED_EDGE('',*,*,#3968,.F.);
#5341=ORIENTED_EDGE('',*,*,#3971,.F.);
#5342=ORIENTED_EDGE('',*,*,#3956,.F.);
#5343=ORIENTED_EDGE('',*,*,#3960,.F.);
#5344=ORIENTED_EDGE('',*,*,#3963,.F.);
#5345=ORIENTED_EDGE('',*,*,#3966,.F.);
#5346=ORIENTED_EDGE('',*,*,#3969,.F.);
#5347=ORIENTED_EDGE('',*,*,#3972,.F.);
#5348=ORIENTED_EDGE('',*,*,#3954,.T.);
#5349=ORIENTED_EDGE('',*,*,#3970,.T.);
#5350=ORIENTED_EDGE('',*,*,#3967,.T.);
#5351=ORIENTED_EDGE('',*,*,#3964,.T.);
#5352=ORIENTED_EDGE('',*,*,#3961,.T.);
#5353=ORIENTED_EDGE('',*,*,#3958,.T.);
#5354=ORIENTED_EDGE('',*,*,#3973,.F.);
#5355=ORIENTED_EDGE('',*,*,#3974,.T.);
#5356=ORIENTED_EDGE('',*,*,#3972,.T.);
#5357=ORIENTED_EDGE('',*,*,#3974,.F.);
#5358=ORIENTED_EDGE('',*,*,#3953,.T.);
#5359=ORIENTED_EDGE('',*,*,#3975,.T.);
#5360=ORIENTED_EDGE('',*,*,#3973,.T.);
#5361=ORIENTED_EDGE('',*,*,#3975,.F.);
#5679=CYLINDRICAL_SURFACE('',#7263,0.1954);
#6007=ADVANCED_FACE('',(#1201),#847,.F.);
#6008=ADVANCED_FACE('',(#1202),#848,.F.);
#6009=ADVANCED_FACE('',(#1203),#849,.F.);
#6010=ADVANCED_FACE('',(#1204),#850,.F.);
#6011=ADVANCED_FACE('',(#1205),#851,.F.);
#6012=ADVANCED_FACE('',(#1206),#852,.F.);
#6013=ADVANCED_FACE('',(#1207),#853,.F.);
#6014=ADVANCED_FACE('',(#1208),#854,.F.);
#6015=ADVANCED_FACE('',(#1209,#681),#855,.T.);
#6016=ADVANCED_FACE('',(#1210),#302,.T.);
#6017=ADVANCED_FACE('',(#1211),#5679,.T.);
#6110=CLOSED_SHELL('',(#6007,#6008,#6009,#6010,#6011,#6012,#6013,#6014,
#6015,#6016,#6017));
#7249=AXIS2_PLACEMENT_3D('',#11506,#9043,#9044);
#7250=AXIS2_PLACEMENT_3D('',#11507,#9045,#9046);
#7251=AXIS2_PLACEMENT_3D('',#11509,#9047,#9048);
#7252=AXIS2_PLACEMENT_3D('',#11510,#9049,#9050);
#7253=AXIS2_PLACEMENT_3D('',#11519,#9055,#9056);
#7254=AXIS2_PLACEMENT_3D('',#11525,#9060,#9061);
#7255=AXIS2_PLACEMENT_3D('',#11531,#9065,#9066);
#7256=AXIS2_PLACEMENT_3D('',#11537,#9070,#9071);
#7257=AXIS2_PLACEMENT_3D('',#11543,#9075,#9076);
#7258=AXIS2_PLACEMENT_3D('',#11546,#9079,#9080);
#7259=AXIS2_PLACEMENT_3D('',#11547,#9081,#9082);
#7260=AXIS2_PLACEMENT_3D('',#11549,#9083,#9084);
#7261=AXIS2_PLACEMENT_3D('',#11550,#9085,#9086);
#7262=AXIS2_PLACEMENT_3D('',#11552,#9087,#9088);
#7263=AXIS2_PLACEMENT_3D('',#11554,#9090,#9091);
#9043=DIRECTION('axis',(0.,0.,1.));
#9044=DIRECTION('refdir',(1.,0.,0.));
#9045=DIRECTION('center_axis',(0.,1.,0.));
#9046=DIRECTION('ref_axis',(1.,0.,0.));
#9047=DIRECTION('center_axis',(0.,1.,0.));
#9048=DIRECTION('ref_axis',(1.,0.,0.));
#9049=DIRECTION('center_axis',(0.866025403784439,0.,-0.5));
#9050=DIRECTION('ref_axis',(0.5,0.,0.866025403784439));
#9051=DIRECTION('',(0.5,0.,0.866025403784439));
#9052=DIRECTION('',(0.,-1.,0.));
#9053=DIRECTION('',(0.5,0.,0.866025403784439));
#9054=DIRECTION('',(0.,-1.,0.));
#9055=DIRECTION('center_axis',(1.20185167898973E-16,0.,-1.));
#9056=DIRECTION('ref_axis',(1.,0.,1.20185167898973E-16));
#9057=DIRECTION('',(1.,0.,1.20185167898973E-16));
#9058=DIRECTION('',(0.,-1.,0.));
#9059=DIRECTION('',(1.,0.,1.20185167898973E-16));
#9060=DIRECTION('center_axis',(-0.866025403784439,0.,-0.5));
#9061=DIRECTION('ref_axis',(0.5,0.,-0.866025403784439));
#9062=DIRECTION('',(0.5,0.,-0.866025403784439));
#9063=DIRECTION('',(0.,-1.,0.));
#9064=DIRECTION('',(0.5,0.,-0.866025403784439));
#9065=DIRECTION('center_axis',(-0.866025403784439,0.,0.5));
#9066=DIRECTION('ref_axis',(-0.5,0.,-0.866025403784439));
#9067=DIRECTION('',(-0.5,0.,-0.866025403784439));
#9068=DIRECTION('',(0.,-1.,0.));
#9069=DIRECTION('',(-0.5,0.,-0.866025403784439));
#9070=DIRECTION('center_axis',(-2.40370335797945E-16,0.,1.));
#9071=DIRECTION('ref_axis',(-1.,0.,-2.40370335797945E-16));
#9072=DIRECTION('',(-1.,0.,-2.40370335797945E-16));
#9073=DIRECTION('',(0.,-1.,0.));
#9074=DIRECTION('',(-1.,0.,-2.40370335797945E-16));
#9075=DIRECTION('center_axis',(0.866025403784439,0.,0.5));
#9076=DIRECTION('ref_axis',(-0.5,0.,0.866025403784439));
#9077=DIRECTION('',(-0.5,0.,0.866025403784439));
#9078=DIRECTION('',(-0.5,0.,0.866025403784439));
#9079=DIRECTION('center_axis',(0.,-1.,0.));
#9080=DIRECTION('ref_axis',(0.,0.,-1.));
#9081=DIRECTION('center_axis',(0.,1.,0.));
#9082=DIRECTION('ref_axis',(0.,0.,1.));
#9083=DIRECTION('center_axis',(0.,-1.,0.));
#9084=DIRECTION('ref_axis',(1.,0.,0.));
#9085=DIRECTION('center_axis',(0.,-1.,0.));
#9086=DIRECTION('ref_axis',(1.,0.,0.));
#9087=DIRECTION('center_axis',(0.,-1.,0.));
#9088=DIRECTION('ref_axis',(1.,0.,0.));
#9089=DIRECTION('',(0.707106781186548,0.707106781186547,8.65956056235494E-17));
#9090=DIRECTION('center_axis',(0.,-1.,0.));
#9091=DIRECTION('ref_axis',(1.,0.,0.));
#9092=DIRECTION('',(0.,1.,0.));
#11506=CARTESIAN_POINT('',(0.,0.,0.));
#11507=CARTESIAN_POINT('Origin',(0.,-0.4,0.));
#11508=CARTESIAN_POINT('',(-0.1954,-0.4,2.39295984553393E-17));
#11509=CARTESIAN_POINT('Origin',(0.,-0.4,0.));
#11510=CARTESIAN_POINT('Origin',(0.0577350269189626,0.,-0.1));
#11511=CARTESIAN_POINT('',(0.0577350269189626,0.,-0.1));
#11512=CARTESIAN_POINT('',(0.115470053837925,0.,0.));
#11513=CARTESIAN_POINT('',(0.0934187836487032,0.,-0.0381939203391614));
#11514=CARTESIAN_POINT('',(0.0577350269189626,-0.2,-0.1));
#11515=CARTESIAN_POINT('',(0.0577350269189626,0.,-0.1));
#11516=CARTESIAN_POINT('',(0.115470053837925,-0.2,0.));
#11517=CARTESIAN_POINT('',(0.115470053837925,-0.2,0.));
#11518=CARTESIAN_POINT('',(0.115470053837925,0.,0.));
#11519=CARTESIAN_POINT('Origin',(-0.0577350269189626,0.,-0.1));
#11520=CARTESIAN_POINT('',(-0.0577350269189626,0.,-0.1));
#11521=CARTESIAN_POINT('',(0.0561324865405187,0.,-0.1));
#11522=CARTESIAN_POINT('',(-0.0577350269189626,-0.2,-0.1));
#11523=CARTESIAN_POINT('',(-0.0577350269189626,0.,-0.1));
#11524=CARTESIAN_POINT('',(0.0577350269189626,-0.2,-0.1));
#11525=CARTESIAN_POINT('Origin',(-0.115470053837925,0.,-1.38777878078145E-17));
#11526=CARTESIAN_POINT('',(-0.115470053837925,0.,-1.41410031829988E-17));
#11527=CARTESIAN_POINT('',(-0.0797862971081845,0.,-0.0618060796608387));
#11528=CARTESIAN_POINT('',(-0.115470053837925,-0.2,-1.38777878078145E-17));
#11529=CARTESIAN_POINT('',(-0.115470053837925,0.,-1.41410031829988E-17));
#11530=CARTESIAN_POINT('',(-0.0577350269189626,-0.2,-0.1));
#11531=CARTESIAN_POINT('Origin',(-0.0577350269189626,0.,0.1));
#11532=CARTESIAN_POINT('',(-0.0577350269189626,0.,0.1));
#11533=CARTESIAN_POINT('',(-0.0509187836487033,0.,0.111806079660839));
#11534=CARTESIAN_POINT('',(-0.0577350269189626,-0.2,0.1));
#11535=CARTESIAN_POINT('',(-0.0577350269189626,0.,0.1));
#11536=CARTESIAN_POINT('',(-0.115470053837925,-0.2,-1.41410031829988E-17));
#11537=CARTESIAN_POINT('Origin',(0.0577350269189626,0.,0.1));
#11538=CARTESIAN_POINT('',(0.0577350269189626,0.,0.1));
#11539=CARTESIAN_POINT('',(0.113867513459481,0.,0.1));
#11540=CARTESIAN_POINT('',(0.0577350269189626,-0.2,0.1));
#11541=CARTESIAN_POINT('',(0.0577350269189626,0.,0.1));
#11542=CARTESIAN_POINT('',(-0.0577350269189626,-0.2,0.1));
#11543=CARTESIAN_POINT('Origin',(0.115470053837925,0.,0.));
#11544=CARTESIAN_POINT('',(0.122286297108185,0.,-0.0118060796608386));
#11545=CARTESIAN_POINT('',(0.0577350269189626,-0.2,0.1));
#11546=CARTESIAN_POINT('Origin',(0.,-0.2,0.));
#11547=CARTESIAN_POINT('Origin',(0.17,0.,0.));
#11548=CARTESIAN_POINT('',(-0.17,-8.67361737988404E-18,-2.0818995585505E-17));
#11549=CARTESIAN_POINT('Origin',(0.,0.,0.));
#11550=CARTESIAN_POINT('Origin',(0.,-0.015,0.));
#11551=CARTESIAN_POINT('',(-0.1954,-0.0254,-2.39295984553393E-17));
#11552=CARTESIAN_POINT('Origin',(0.,-0.0254,0.));
#11553=CARTESIAN_POINT('',(-0.185,-0.015,-2.2655965784226E-17));
#11554=CARTESIAN_POINT('Origin',(0.,-0.2775,0.));
#11555=CARTESIAN_POINT('',(-0.1954,-0.2775,-2.39295984553393E-17));
#11862=UNCERTAINTY_MEASURE_WITH_UNIT(LENGTH_MEASURE(0.001),#11917,
'DISTANCE_ACCURACY_VALUE',
'Maximum model space distance between geometric entities at asserted c
onnectivities');
#11869=UNCERTAINTY_MEASURE_WITH_UNIT(LENGTH_MEASURE(0.001),#11917,
'DISTANCE_ACCURACY_VALUE',
'Maximum model space distance between geometric entities at asserted c
onnectivities');
#11909=(
GEOMETRIC_REPRESENTATION_CONTEXT(3)
GLOBAL_UNCERTAINTY_ASSIGNED_CONTEXT((#11862))
GLOBAL_UNIT_ASSIGNED_CONTEXT((#11917,#11919,#11920))
REPRESENTATION_CONTEXT('','3D')
);
#11916=(
GEOMETRIC_REPRESENTATION_CONTEXT(3)
GLOBAL_UNCERTAINTY_ASSIGNED_CONTEXT((#11869))
GLOBAL_UNIT_ASSIGNED_CONTEXT((#11917,#11919,#11920))
REPRESENTATION_CONTEXT('','3D')
);
#11917=(
LENGTH_UNIT()
NAMED_UNIT(*)
SI_UNIT(.CENTI.,.METRE.)
);
#11919=(
NAMED_UNIT(*)
PLANE_ANGLE_UNIT()
SI_UNIT($,.RADIAN.)
);
#11920=(
NAMED_UNIT(*)
SI_UNIT($,.STERADIAN.)
SOLID_ANGLE_UNIT()
);
#11960=SHAPE_DEFINITION_REPRESENTATION(#12011,#12118);
#12011=PRODUCT_DEFINITION_SHAPE('',$,#12165);
#12118=SHAPE_REPRESENTATION('',(#7249),#11909);
#12125=PRODUCT_DEFINITION_CONTEXT('part definition',#12265,'design');
#12165=PRODUCT_DEFINITION('M4x4 collar screw','M4x4 collar screw',#12211,
#12125);
#12211=PRODUCT_DEFINITION_FORMATION('',$,#12306);
#12265=APPLICATION_CONTEXT(
'Core Data for Automotive Mechanical Design Process');
#12266=PRODUCT_CONTEXT('part definition',#12265,'mechanical');
#12306=PRODUCT('M4x4 collar screw','M4x4 collar screw',
'M4x4 collar screw',(#12266));
#12376=COLOUR_RGB('Black',0.12,0.14,0.17);
#12377=FILL_AREA_STYLE_COLOUR('',#12376);
#12378=FILL_AREA_STYLE('',(#12377));
#12379=SURFACE_STYLE_FILL_AREA(#12378);
#12380=SURFACE_SIDE_STYLE('',(#12379));
#12381=SURFACE_STYLE_USAGE(.BOTH.,#12380);
#12382=PRESENTATION_STYLE_ASSIGNMENT((#12381));
ENDSEC;
END-ISO-10303-21;
